ISO-10303-21;
HEADER;
/* Generated by software containing ST-Developer
 * from STEP Tools, Inc. (www.steptools.com) 
 */

FILE_DESCRIPTION(
/* description */ ('Bearing friction torque test rig'),
/* implementation_level */ '2;1');

FILE_NAME(
/* name */ 'M4x10 Cap Screw.step',
/* time_stamp */ '2026-10-28T03:24:04-07:00',
/* author */ (''),
/* organization */ (''),
/* preprocessor_version */ 'ST-DEVELOPER v20.2',
/* originating_system */ 'Autodesk Translation Framework v15.17.0.0',
/* authorisation */ '');

FILE_SCHEMA (('AUTOMOTIVE_DESIGN { 1 0 10303 214 3 1 1 }'));
ENDSEC;

DATA;
#10=MECHANICAL_DESIGN_GEOMETRIC_PRESENTATION_REPRESENTATION('',(#581),#14822);
#444=CONICAL_SURFACE('',#8923,0.325,0.785398163397448);
#445=CONICAL_SURFACE('',#8927,0.335,0.785398163397448);
#446=CONICAL_SURFACE('',#8931,0.21,0.463647609000806);
#451=ORIENTED_CLOSED_SHELL('',*,#7699,.F.);
#454=BREP_WITH_VOIDS('Body1',#7700,(#451));
#488=SHAPE_REPRESENTATION_RELATIONSHIP('SRR','None',#15029,#527);
#527=ADVANCED_BREP_SHAPE_REPRESENTATION('',(#454),#14809);
#581=STYLED_ITEM('',(#15291),#454);
#833=FACE_BOUND('',#2100,.T.);
#1046=PLANE('',#8911);
#1047=PLANE('',#8912);
#1048=PLANE('',#8913);
#1049=PLANE('',#8914);
#1050=PLANE('',#8915);
#1051=PLANE('',#8916);
#1052=PLANE('',#8917);
#1053=PLANE('',#8918);
#1054=PLANE('',#8919);
#1055=PLANE('',#8921);
#1056=PLANE('',#8929);
#1452=FACE_OUTER_BOUND('',#2086,.T.);
#1453=FACE_OUTER_BOUND('',#2087,.T.);
#1454=FACE_OUTER_BOUND('',#2088,.T.);
#1455=FACE_OUTER_BOUND('',#2089,.T.);
#1456=FACE_OUTER_BOUND('',#2090,.T.);
#1457=FACE_OUTER_BOUND('',#2091,.T.);
#1458=FACE_OUTER_BOUND('',#2092,.T.);
#1459=FACE_OUTER_BOUND('',#2093,.T.);
#1460=FACE_OUTER_BOUND('',#2094,.T.);
#1461=FACE_OUTER_BOUND('',#2095,.T.);
#1462=FACE_OUTER_BOUND('',#2096,.T.);
#1463=FACE_OUTER_BOUND('',#2097,.T.);
#1464=FACE_OUTER_BOUND('',#2098,.T.);
#1465=FACE_OUTER_BOUND('',#2099,.T.);
#1466=FACE_OUTER_BOUND('',#2101,.T.);
#1467=FACE_OUTER_BOUND('',#2102,.T.);
#2086=EDGE_LOOP('',(#6678,#6679,#6680,#6681));
#2087=EDGE_LOOP('',(#6682,#6683,#6684,#6685));
#2088=EDGE_LOOP('',(#6686,#6687,#6688,#6689));
#2089=EDGE_LOOP('',(#6690,#6691,#6692,#6693));
#2090=EDGE_LOOP('',(#6694,#6695,#6696,#6697));
#2091=EDGE_LOOP('',(#6698,#6699,#6700,#6701));
#2092=EDGE_LOOP('',(#6702,#6703,#6704,#6705,#6706,#6707));
#2093=EDGE_LOOP('',(#6708,#6709,#6710,#6711,#6712,#6713));
#2094=EDGE_LOOP('',(#6714));
#2095=EDGE_LOOP('',(#6715));
#2096=EDGE_LOOP('',(#6716,#6717,#6718,#6719));
#2097=EDGE_LOOP('',(#6720,#6721,#6722,#6723));
#2098=EDGE_LOOP('',(#6724,#6725,#6726,#6727));
#2099=EDGE_LOOP('',(#6728));
#2100=EDGE_LOOP('',(#6729));
#2101=EDGE_LOOP('',(#6730,#6731,#6732,#6733));
#2102=EDGE_LOOP('',(#6734,#6735,#6736,#6737));
#2578=LINE('',#13978,#3022);
#2579=LINE('',#13980,#3023);
#2580=LINE('',#13982,#3024);
#2581=LINE('',#13983,#3025);
#2582=LINE('',#13986,#3026);
#2583=LINE('',#13988,#3027);
#2584=LINE('',#13989,#3028);
#2585=LINE('',#13992,#3029);
#2586=LINE('',#13994,#3030);
#2587=LINE('',#13995,#3031);
#2588=LINE('',#13998,#3032);
#2589=LINE('',#14000,#3033);
#2590=LINE('',#14001,#3034);
#2591=LINE('',#14004,#3035);
#2592=LINE('',#14006,#3036);
#2593=LINE('',#14007,#3037);
#2594=LINE('',#14009,#3038);
#2595=LINE('',#14010,#3039);
#2596=LINE('',#14022,#3040);
#2597=LINE('',#14026,#3041);
#2598=LINE('',#14030,#3042);
#2599=LINE('',#14037,#3043);
#2600=LINE('',#14039,#3044);
#3022=VECTOR('',#11065,1.);
#3023=VECTOR('',#11066,1.);
#3024=VECTOR('',#11067,1.);
#3025=VECTOR('',#11068,1.);
#3026=VECTOR('',#11071,1.);
#3027=VECTOR('',#11072,1.);
#3028=VECTOR('',#11073,1.);
#3029=VECTOR('',#11076,1.);
#3030=VECTOR('',#11077,1.);
#3031=VECTOR('',#11078,1.);
#3032=VECTOR('',#11081,1.);
#3033=VECTOR('',#11082,1.);
#3034=VECTOR('',#11083,1.);
#3035=VECTOR('',#11086,1.);
#3036=VECTOR('',#11087,1.);
#3037=VECTOR('',#11088,1.);
#3038=VECTOR('',#11091,1.);
#3039=VECTOR('',#11092,1.);
#3040=VECTOR('',#11109,0.325);
#3041=VECTOR('',#11114,0.35);
#3042=VECTOR('',#11119,0.335);
#3043=VECTOR('',#11128,0.21);
#3044=VECTOR('',#11131,0.2);
#3475=CIRCLE('',#8920,0.1954);
#3476=CIRCLE('',#8922,0.3);
#3477=CIRCLE('',#8924,0.35);
#3478=CIRCLE('',#8926,0.35);
#3479=CIRCLE('',#8928,0.32);
#3480=CIRCLE('',#8930,0.22);
#3481=CIRCLE('',#8932,0.1954);
#4078=VERTEX_POINT('',#13976);
#4079=VERTEX_POINT('',#13977);
#4080=VERTEX_POINT('',#13979);
#4081=VERTEX_POINT('',#13981);
#4082=VERTEX_POINT('',#13985);
#4083=VERTEX_POINT('',#13987);
#4084=VERTEX_POINT('',#13991);
#4085=VERTEX_POINT('',#13993);
#4086=VERTEX_POINT('',#13997);
#4087=VERTEX_POINT('',#13999);
#4088=VERTEX_POINT('',#14003);
#4089=VERTEX_POINT('',#14005);
#4090=VERTEX_POINT('',#14014);
#4091=VERTEX_POINT('',#14017);
#4092=VERTEX_POINT('',#14020);
#4093=VERTEX_POINT('',#14024);
#4094=VERTEX_POINT('',#14028);
#4095=VERTEX_POINT('',#14032);
#4096=VERTEX_POINT('',#14035);
#4965=EDGE_CURVE('',#4078,#4079,#2578,.T.);
#4966=EDGE_CURVE('',#4079,#4080,#2579,.T.);
#4967=EDGE_CURVE('',#4080,#4081,#2580,.T.);
#4968=EDGE_CURVE('',#4078,#4081,#2581,.T.);
#4969=EDGE_CURVE('',#4079,#4082,#2582,.T.);
#4970=EDGE_CURVE('',#4082,#4083,#2583,.T.);
#4971=EDGE_CURVE('',#4083,#4080,#2584,.T.);
#4972=EDGE_CURVE('',#4082,#4084,#2585,.T.);
#4973=EDGE_CURVE('',#4084,#4085,#2586,.T.);
#4974=EDGE_CURVE('',#4085,#4083,#2587,.T.);
#4975=EDGE_CURVE('',#4084,#4086,#2588,.T.);
#4976=EDGE_CURVE('',#4086,#4087,#2589,.T.);
#4977=EDGE_CURVE('',#4087,#4085,#2590,.T.);
#4978=EDGE_CURVE('',#4086,#4088,#2591,.T.);
#4979=EDGE_CURVE('',#4088,#4089,#2592,.T.);
#4980=EDGE_CURVE('',#4089,#4087,#2593,.T.);
#4981=EDGE_CURVE('',#4088,#4078,#2594,.T.);
#4982=EDGE_CURVE('',#4081,#4089,#2595,.T.);
#4983=EDGE_CURVE('',#4090,#4090,#3475,.T.);
#4984=EDGE_CURVE('',#4091,#4091,#3476,.T.);
#4985=EDGE_CURVE('',#4092,#4092,#3477,.T.);
#4986=EDGE_CURVE('',#4092,#4091,#2596,.T.);
#4987=EDGE_CURVE('',#4093,#4093,#3478,.T.);
#4988=EDGE_CURVE('',#4093,#4092,#2597,.T.);
#4989=EDGE_CURVE('',#4094,#4094,#3479,.T.);
#4990=EDGE_CURVE('',#4094,#4093,#2598,.T.);
#4991=EDGE_CURVE('',#4095,#4095,#3480,.T.);
#4992=EDGE_CURVE('',#4096,#4096,#3481,.F.);
#4993=EDGE_CURVE('',#4096,#4095,#2599,.T.);
#4994=EDGE_CURVE('',#4090,#4096,#2600,.T.);
#6678=ORIENTED_EDGE('',*,*,#4965,.T.);
#6679=ORIENTED_EDGE('',*,*,#4966,.T.);
#6680=ORIENTED_EDGE('',*,*,#4967,.T.);
#6681=ORIENTED_EDGE('',*,*,#4968,.F.);
#6682=ORIENTED_EDGE('',*,*,#4969,.T.);
#6683=ORIENTED_EDGE('',*,*,#4970,.T.);
#6684=ORIENTED_EDGE('',*,*,#4971,.T.);
#6685=ORIENTED_EDGE('',*,*,#4966,.F.);
#6686=ORIENTED_EDGE('',*,*,#4972,.T.);
#6687=ORIENTED_EDGE('',*,*,#4973,.T.);
#6688=ORIENTED_EDGE('',*,*,#4974,.T.);
#6689=ORIENTED_EDGE('',*,*,#4970,.F.);
#6690=ORIENTED_EDGE('',*,*,#4975,.T.);
#6691=ORIENTED_EDGE('',*,*,#4976,.T.);
#6692=ORIENTED_EDGE('',*,*,#4977,.T.);
#6693=ORIENTED_EDGE('',*,*,#4973,.F.);
#6694=ORIENTED_EDGE('',*,*,#4978,.T.);
#6695=ORIENTED_EDGE('',*,*,#4979,.T.);
#6696=ORIENTED_EDGE('',*,*,#4980,.T.);
#6697=ORIENTED_EDGE('',*,*,#4976,.F.);
#6698=ORIENTED_EDGE('',*,*,#4981,.T.);
#6699=ORIENTED_EDGE('',*,*,#4968,.T.);
#6700=ORIENTED_EDGE('',*,*,#4982,.T.);
#6701=ORIENTED_EDGE('',*,*,#4979,.F.);
#6702=ORIENTED_EDGE('',*,*,#4981,.F.);
#6703=ORIENTED_EDGE('',*,*,#4978,.F.);
#6704=ORIENTED_EDGE('',*,*,#4975,.F.);
#6705=ORIENTED_EDGE('',*,*,#4972,.F.);
#6706=ORIENTED_EDGE('',*,*,#4969,.F.);
#6707=ORIENTED_EDGE('',*,*,#4965,.F.);
#6708=ORIENTED_EDGE('',*,*,#4982,.F.);
#6709=ORIENTED_EDGE('',*,*,#4967,.F.);
#6710=ORIENTED_EDGE('',*,*,#4971,.F.);
#6711=ORIENTED_EDGE('',*,*,#4974,.F.);
#6712=ORIENTED_EDGE('',*,*,#4977,.F.);
#6713=ORIENTED_EDGE('',*,*,#4980,.F.);
#6714=ORIENTED_EDGE('',*,*,#4983,.F.);
#6715=ORIENTED_EDGE('',*,*,#4984,.F.);
#6716=ORIENTED_EDGE('',*,*,#4985,.F.);
#6717=ORIENTED_EDGE('',*,*,#4986,.T.);
#6718=ORIENTED_EDGE('',*,*,#4984,.T.);
#6719=ORIENTED_EDGE('',*,*,#4986,.F.);
#6720=ORIENTED_EDGE('',*,*,#4987,.F.);
#6721=ORIENTED_EDGE('',*,*,#4988,.T.);
#6722=ORIENTED_EDGE('',*,*,#4985,.T.);
#6723=ORIENTED_EDGE('',*,*,#4988,.F.);
#6724=ORIENTED_EDGE('',*,*,#4989,.F.);
#6725=ORIENTED_EDGE('',*,*,#4990,.T.);
#6726=ORIENTED_EDGE('',*,*,#4987,.T.);
#6727=ORIENTED_EDGE('',*,*,#4990,.F.);
#6728=ORIENTED_EDGE('',*,*,#4989,.T.);
#6729=ORIENTED_EDGE('',*,*,#4991,.F.);
#6730=ORIENTED_EDGE('',*,*,#4992,.F.);
#6731=ORIENTED_EDGE('',*,*,#4993,.T.);
#6732=ORIENTED_EDGE('',*,*,#4991,.T.);
#6733=ORIENTED_EDGE('',*,*,#4993,.F.);
#6734=ORIENTED_EDGE('',*,*,#4983,.T.);
#6735=ORIENTED_EDGE('',*,*,#4994,.T.);
#6736=ORIENTED_EDGE('',*,*,#4992,.T.);
#6737=ORIENTED_EDGE('',*,*,#4994,.F.);
#7176=CYLINDRICAL_SURFACE('',#8925,0.35);
#7177=CYLINDRICAL_SURFACE('',#8933,0.1954);
#7563=ADVANCED_FACE('',(#1452),#1046,.F.);
#7564=ADVANCED_FACE('',(#1453),#1047,.F.);
#7565=ADVANCED_FACE('',(#1454),#1048,.F.);
#7566=ADVANCED_FACE('',(#1455),#1049,.F.);
#7567=ADVANCED_FACE('',(#1456),#1050,.F.);
#7568=ADVANCED_FACE('',(#1457),#1051,.F.);
#7569=ADVANCED_FACE('',(#1458),#1052,.F.);
#7570=ADVANCED_FACE('',(#1459),#1053,.F.);
#7571=ADVANCED_FACE('',(#1460),#1054,.F.);
#7572=ADVANCED_FACE('',(#1461),#1055,.T.);
#7573=ADVANCED_FACE('',(#1462),#444,.T.);
#7574=ADVANCED_FACE('',(#1463),#7176,.T.);
#7575=ADVANCED_FACE('',(#1464),#445,.T.);
#7576=ADVANCED_FACE('',(#1465,#833),#1056,.T.);
#7577=ADVANCED_FACE('',(#1466),#446,.T.);
#7578=ADVANCED_FACE('',(#1467),#7177,.T.);
#7699=CLOSED_SHELL('',(#7563,#7564,#7565,#7566,#7567,#7568,#7569,#7570));
#7700=CLOSED_SHELL('',(#7571,#7572,#7573,#7574,#7575,#7576,#7577,#7578));
#8910=AXIS2_PLACEMENT_3D('',#13974,#11061,#11062);
#8911=AXIS2_PLACEMENT_3D('',#13975,#11063,#11064);
#8912=AXIS2_PLACEMENT_3D('',#13984,#11069,#11070);
#8913=AXIS2_PLACEMENT_3D('',#13990,#11074,#11075);
#8914=AXIS2_PLACEMENT_3D('',#13996,#11079,#11080);
#8915=AXIS2_PLACEMENT_3D('',#14002,#11084,#11085);
#8916=AXIS2_PLACEMENT_3D('',#14008,#11089,#11090);
#8917=AXIS2_PLACEMENT_3D('',#14011,#11093,#11094);
#8918=AXIS2_PLACEMENT_3D('',#14012,#11095,#11096);
#8919=AXIS2_PLACEMENT_3D('',#14013,#11097,#11098);
#8920=AXIS2_PLACEMENT_3D('',#14015,#11099,#11100);
#8921=AXIS2_PLACEMENT_3D('',#14016,#11101,#11102);
#8922=AXIS2_PLACEMENT_3D('',#14018,#11103,#11104);
#8923=AXIS2_PLACEMENT_3D('',#14019,#11105,#11106);
#8924=AXIS2_PLACEMENT_3D('',#14021,#11107,#11108);
#8925=AXIS2_PLACEMENT_3D('',#14023,#11110,#11111);
#8926=AXIS2_PLACEMENT_3D('',#14025,#11112,#11113);
#8927=AXIS2_PLACEMENT_3D('',#14027,#11115,#11116);
#8928=AXIS2_PLACEMENT_3D('',#14029,#11117,#11118);
#8929=AXIS2_PLACEMENT_3D('',#14031,#11120,#11121);
#8930=AXIS2_PLACEMENT_3D('',#14033,#11122,#11123);
#8931=AXIS2_PLACEMENT_3D('',#14034,#11124,#11125);
#8932=AXIS2_PLACEMENT_3D('',#14036,#11126,#11127);
#8933=AXIS2_PLACEMENT_3D('',#14038,#11129,#11130);
#11061=DIRECTION('axis',(0.,0.,1.));
#11062=DIRECTION('refdir',(1.,0.,0.));
#11063=DIRECTION('center_axis',(0.866025403784439,0.,-0.5));
#11064=DIRECTION('ref_axis',(0.5,0.,0.866025403784439));
#11065=DIRECTION('',(-0.5,0.,-0.866025403784439));
#11066=DIRECTION('',(0.,-1.,0.));
#11067=DIRECTION('',(0.5,0.,0.866025403784439));
#11068=DIRECTION('',(0.,-1.,0.));
#11069=DIRECTION('center_axis',(1.60246890531964E-16,0.,-1.));
#11070=DIRECTION('ref_axis',(1.,0.,1.60246890531964E-16));
#11071=DIRECTION('',(-1.,0.,-1.60246890531964E-16));
#11072=DIRECTION('',(0.,-1.,0.));
#11073=DIRECTION('',(1.,0.,1.60246890531964E-16));
#11074=DIRECTION('center_axis',(-0.866025403784439,0.,-0.5));
#11075=DIRECTION('ref_axis',(0.5,0.,-0.866025403784439));
#11076=DIRECTION('',(-0.5,0.,0.866025403784439));
#11077=DIRECTION('',(0.,-1.,0.));
#11078=DIRECTION('',(0.5,0.,-0.866025403784439));
#11079=DIRECTION('center_axis',(-0.866025403784439,0.,0.5));
#11080=DIRECTION('ref_axis',(-0.5,0.,-0.866025403784439));
#11081=DIRECTION('',(0.5,0.,0.866025403784439));
#11082=DIRECTION('',(0.,-1.,0.));
#11083=DIRECTION('',(-0.5,0.,-0.866025403784439));
#11084=DIRECTION('center_axis',(-1.60246890531964E-16,0.,1.));
#11085=DIRECTION('ref_axis',(-1.,0.,-1.60246890531964E-16));
#11086=DIRECTION('',(1.,0.,1.60246890531964E-16));
#11087=DIRECTION('',(0.,-1.,0.));
#11088=DIRECTION('',(-1.,0.,-1.60246890531964E-16));
#11089=DIRECTION('center_axis',(0.866025403784439,0.,0.5));
#11090=DIRECTION('ref_axis',(-0.5,0.,0.866025403784439));
#11091=DIRECTION('',(0.5,0.,-0.866025403784439));
#11092=DIRECTION('',(-0.5,0.,0.866025403784439));
#11093=DIRECTION('center_axis',(0.,1.,0.));
#11094=DIRECTION('ref_axis',(1.,0.,0.));
#11095=DIRECTION('center_axis',(0.,-1.,0.));
#11096=DIRECTION('ref_axis',(0.,0.,-1.));
#11097=DIRECTION('center_axis',(0.,1.,0.));
#11098=DIRECTION('ref_axis',(1.,0.,0.));
#11099=DIRECTION('center_axis',(0.,1.,0.));
#11100=DIRECTION('ref_axis',(1.,0.,0.));
#11101=DIRECTION('center_axis',(0.,1.,0.));
#11102=DIRECTION('ref_axis',(0.,0.,1.));
#11103=DIRECTION('center_axis',(0.,-1.,0.));
#11104=DIRECTION('ref_axis',(1.,0.,0.));
#11105=DIRECTION('center_axis',(0.,-1.,0.));
#11106=DIRECTION('ref_axis',(1.,0.,0.));
#11107=DIRECTION('center_axis',(0.,-1.,0.));
#11108=DIRECTION('ref_axis',(1.,0.,0.));
#11109=DIRECTION('',(0.707106781186547,0.707106781186548,8.65956056235493E-17));
#11110=DIRECTION('center_axis',(0.,-1.,0.));
#11111=DIRECTION('ref_axis',(1.,0.,0.));
#11112=DIRECTION('center_axis',(0.,-1.,0.));
#11113=DIRECTION('ref_axis',(1.,0.,0.));
#11114=DIRECTION('',(0.,1.,0.));
#11115=DIRECTION('center_axis',(0.,1.,0.));
#11116=DIRECTION('ref_axis',(1.,0.,0.));
#11117=DIRECTION('center_axis',(0.,-1.,0.));
#11118=DIRECTION('ref_axis',(1.,0.,0.));
#11119=DIRECTION('',(-0.707106781186547,0.707106781186548,-8.65956056235493E-17));
#11120=DIRECTION('center_axis',(0.,-1.,0.));
#11121=DIRECTION('ref_axis',(0.,0.,-1.));
#11122=DIRECTION('center_axis',(0.,-1.,0.));
#11123=DIRECTION('ref_axis',(1.,0.,0.));
#11124=DIRECTION('center_axis',(0.,1.,0.));
#11125=DIRECTION('ref_axis',(1.,0.,0.));
#11126=DIRECTION('center_axis',(0.,1.,0.));
#11127=DIRECTION('ref_axis',(1.,0.,0.));
#11128=DIRECTION('',(-0.447213595499958,0.894427190999916,-5.47678698264203E-17));
#11129=DIRECTION('center_axis',(0.,-1.,0.));
#11130=DIRECTION('ref_axis',(1.,0.,0.));
#11131=DIRECTION('',(0.,1.,0.));
#13974=CARTESIAN_POINT('',(0.,0.,0.));
#13975=CARTESIAN_POINT('Origin',(0.0866025403784439,-0.4,-0.15));
#13976=CARTESIAN_POINT('',(0.173205080756888,-0.4,0.));
#13977=CARTESIAN_POINT('',(0.0866025403784439,-0.4,-0.15));
#13978=CARTESIAN_POINT('',(0.173205080756888,-0.4,0.));
#13979=CARTESIAN_POINT('',(0.0866025403784439,-0.64,-0.15));
#13980=CARTESIAN_POINT('',(0.0866025403784439,-0.4,-0.15));
#13981=CARTESIAN_POINT('',(0.173205080756888,-0.64,0.));
#13982=CARTESIAN_POINT('',(0.173205080756888,-0.64,0.));
#13983=CARTESIAN_POINT('',(0.173205080756888,-0.4,0.));
#13984=CARTESIAN_POINT('Origin',(-0.0866025403784438,-0.4,-0.15));
#13985=CARTESIAN_POINT('',(-0.0866025403784438,-0.4,-0.15));
#13986=CARTESIAN_POINT('',(0.0866025403784439,-0.4,-0.15));
#13987=CARTESIAN_POINT('',(-0.0866025403784438,-0.64,-0.15));
#13988=CARTESIAN_POINT('',(-0.0866025403784438,-0.4,-0.15));
#13989=CARTESIAN_POINT('',(0.0866025403784439,-0.64,-0.15));
#13990=CARTESIAN_POINT('Origin',(-0.173205080756888,-0.4,-2.77555756156289E-17));
#13991=CARTESIAN_POINT('',(-0.173205080756888,-0.4,-2.12115047744981E-17));
#13992=CARTESIAN_POINT('',(-0.0866025403784438,-0.4,-0.15));
#13993=CARTESIAN_POINT('',(-0.173205080756888,-0.64,-2.77555756156289E-17));
#13994=CARTESIAN_POINT('',(-0.173205080756888,-0.4,-2.12115047744981E-17));
#13995=CARTESIAN_POINT('',(-0.0866025403784438,-0.64,-0.15));
#13996=CARTESIAN_POINT('Origin',(-0.0866025403784439,-0.4,0.15));
#13997=CARTESIAN_POINT('',(-0.0866025403784439,-0.4,0.15));
#13998=CARTESIAN_POINT('',(-0.173205080756888,-0.4,-2.12115047744981E-17));
#13999=CARTESIAN_POINT('',(-0.0866025403784439,-0.64,0.15));
#14000=CARTESIAN_POINT('',(-0.0866025403784439,-0.4,0.15));
#14001=CARTESIAN_POINT('',(-0.173205080756888,-0.64,-2.12115047744981E-17));
#14002=CARTESIAN_POINT('Origin',(0.0866025403784439,-0.4,0.15));
#14003=CARTESIAN_POINT('',(0.0866025403784439,-0.4,0.15));
#14004=CARTESIAN_POINT('',(-0.0866025403784439,-0.4,0.15));
#14005=CARTESIAN_POINT('',(0.0866025403784439,-0.64,0.15));
#14006=CARTESIAN_POINT('',(0.0866025403784439,-0.4,0.15));
#14007=CARTESIAN_POINT('',(-0.0866025403784439,-0.64,0.15));
#14008=CARTESIAN_POINT('Origin',(0.173205080756888,-0.4,0.));
#14009=CARTESIAN_POINT('',(0.0866025403784439,-0.4,0.15));
#14010=CARTESIAN_POINT('',(0.0866025403784439,-0.64,0.15));
#14011=CARTESIAN_POINT('Origin',(0.,-0.4,-2.77555756156289E-17));
#14012=CARTESIAN_POINT('Origin',(0.,-0.64,-2.77555756156289E-17));
#14013=CARTESIAN_POINT('Origin',(0.,-1.,0.));
#14014=CARTESIAN_POINT('',(-0.1954,-1.,2.39295984553393E-17));
#14015=CARTESIAN_POINT('Origin',(0.,-1.,0.));
#14016=CARTESIAN_POINT('Origin',(0.3,0.4,0.));
#14017=CARTESIAN_POINT('',(-0.3,0.4,-3.67394039744206E-17));
#14018=CARTESIAN_POINT('Origin',(0.,0.4,0.));
#14019=CARTESIAN_POINT('Origin',(0.,0.375,0.));
#14020=CARTESIAN_POINT('',(-0.35,0.35,-4.28626379701573E-17));
#14021=CARTESIAN_POINT('Origin',(0.,0.35,0.));
#14022=CARTESIAN_POINT('',(-0.325,0.375,-3.9801020972289E-17));
#14023=CARTESIAN_POINT('Origin',(0.,0.19,0.));
#14024=CARTESIAN_POINT('',(-0.35,0.03,-4.28626379701574E-17));
#14025=CARTESIAN_POINT('Origin',(0.,0.03,0.));
#14026=CARTESIAN_POINT('',(-0.35,0.19,-4.28626379701574E-17));
#14027=CARTESIAN_POINT('Origin',(0.,0.0149999999999999,0.));
#14028=CARTESIAN_POINT('',(-0.32,-3.29597460435593E-17,-3.91886975727153E-17));
#14029=CARTESIAN_POINT('Origin',(0.,0.,0.));
#14030=CARTESIAN_POINT('',(-0.335,0.0149999999999999,-4.10256677714363E-17));
#14031=CARTESIAN_POINT('Origin',(0.22,0.,0.));
#14032=CARTESIAN_POINT('',(-0.22,-6.93889390390723E-18,-2.69422295812418E-17));
#14033=CARTESIAN_POINT('Origin',(0.,0.,0.));
#14034=CARTESIAN_POINT('Origin',(0.,-0.02,0.));
#14035=CARTESIAN_POINT('',(-0.1954,-0.0492,2.39295984553393E-17));
#14036=CARTESIAN_POINT('Origin',(0.,-0.0492,0.));
#14037=CARTESIAN_POINT('',(-0.21,-0.02,-2.57175827820944E-17));
#14038=CARTESIAN_POINT('Origin',(0.,-0.8,0.));
#14039=CARTESIAN_POINT('',(-0.1954,-0.8,-2.39295984553393E-17));
#14764=UNCERTAINTY_MEASURE_WITH_UNIT(LENGTH_MEASURE(0.001),#14823,
'DISTANCE_ACCURACY_VALUE',
'Maximum model space distance between geometric entities at asserted c
onnectivities');
#14777=UNCERTAINTY_MEASURE_WITH_UNIT(LENGTH_MEASURE(0.001),#14823,
'DISTANCE_ACCURACY_VALUE',
'Maximum model space distance between geometric entities at asserted c
onnectivities');
#14809=(
GEOMETRIC_REPRESENTATION_CONTEXT(3)
GLOBAL_UNCERTAINTY_ASSIGNED_CONTEXT((#14764))
GLOBAL_UNIT_ASSIGNED_CONTEXT((#14823,#14825,#14826))
REPRESENTATION_CONTEXT('','3D')
);
#14822=(
GEOMETRIC_REPRESENTATION_CONTEXT(3)
GLOBAL_UNCERTAINTY_ASSIGNED_CONTEXT((#14777))
GLOBAL_UNIT_ASSIGNED_CONTEXT((#14823,#14825,#14826))
REPRESENTATION_CONTEXT('','3D')
);
#14823=(
LENGTH_UNIT()
NAMED_UNIT(*)
SI_UNIT(.CENTI.,.METRE.)
);
#14825=(
NAMED_UNIT(*)
PLANE_ANGLE_UNIT()
SI_UNIT($,.RADIAN.)
);
#14826=(
NAMED_UNIT(*)
SI_UNIT($,.STERADIAN.)
SOLID_ANGLE_UNIT()
);
#14858=SHAPE_DEFINITION_REPRESENTATION(#14912,#15029);
#14912=PRODUCT_DEFINITION_SHAPE('',$,#15074);
#15029=SHAPE_REPRESENTATION('',(#8910),#14809);
#15042=PRODUCT_DEFINITION_CONTEXT('part definition',#15176,'design');
#15074=PRODUCT_DEFINITION('M4x10 Cap Screw','M4x10 Cap Screw',#15118,#15042);
#15118=PRODUCT_DEFINITION_FORMATION('',$,#15209);
#15176=APPLICATION_CONTEXT(
'Core Data for Automotive Mechanical Design Process');
#15177=PRODUCT_CONTEXT('part definition',#15176,'mechanical');
#15209=PRODUCT('M4x10 Cap Screw','M4x10 Cap Screw','M4x10 Cap Screw',(#15177));
#15285=COLOUR_RGB('Black',0.12,0.14,0.17);
#15286=FILL_AREA_STYLE_COLOUR('',#15285);
#15287=FILL_AREA_STYLE('',(#15286));
#15288=SURFACE_STYLE_FILL_AREA(#15287);
#15289=SURFACE_SIDE_STYLE('',(#15288));
#15290=SURFACE_STYLE_USAGE(.BOTH.,#15289);
#15291=PRESENTATION_STYLE_ASSIGNMENT((#15290));
ENDSEC;
END-ISO-10303-21;
